ISO-10303-21;
HEADER;
/* Generated by software containing ST-Developer
 * from STEP Tools, Inc. (www.steptools.com) 
 */

FILE_DESCRIPTION(
/* description */ ('Belt tension measurement rig'),
/* implementation_level */ '2;1');

FILE_NAME(
/* name */ 'Cap Screw - M4x16.step',
/* time_stamp */ '2026-10-28T03:24:44-07:00',
/* author */ (''),
/* organization */ (''),
/* preprocessor_version */ 'ST-DEVELOPER v20.2',
/* originating_system */ 'Autodesk Translation Framework v15.17.0.0',
/* authorisation */ '');

FILE_SCHEMA (('AUTOMOTIVE_DESIGN { 1 0 10303 214 3 1 1 }'));
ENDSEC;

DATA;
#10=MECHANICAL_DESIGN_GEOMETRIC_PRESENTATION_REPRESENTATION('',(#758),#23587);
#13=ORIENTED_CLOSED_SHELL('',*,#12266,.F.);
#16=BREP_WITH_VOIDS('Body1',#12265,(#13));
#481=CONICAL_SURFACE('',#14336,0.325,0.785398163397448);
#482=CONICAL_SURFACE('',#14340,0.335,0.785398163397448);
#483=CONICAL_SURFACE('',#14344,0.21,0.463647609000806);
#484=CONICAL_SURFACE('',#14348,0.18,0.785398163397448);
#633=SHAPE_REPRESENTATION_RELATIONSHIP('SRR','None',#23884,#688);
#688=ADVANCED_BREP_SHAPE_REPRESENTATION('',(#16),#23582);
#758=STYLED_ITEM('',(#24218),#16);
#1026=FACE_BOUND('',#2909,.T.);
#1319=PLANE('',#14334);
#1320=PLANE('',#14342);
#1321=PLANE('',#14350);
#1322=PLANE('',#14351);
#1323=PLANE('',#14352);
#1324=PLANE('',#14353);
#1325=PLANE('',#14354);
#1326=PLANE('',#14355);
#1327=PLANE('',#14356);
#1328=PLANE('',#14357);
#1329=PLANE('',#14358);
#2003=FACE_OUTER_BOUND('',#2904,.T.);
#2004=FACE_OUTER_BOUND('',#2905,.T.);
#2005=FACE_OUTER_BOUND('',#2906,.T.);
#2006=FACE_OUTER_BOUND('',#2907,.T.);
#2007=FACE_OUTER_BOUND('',#2908,.T.);
#2008=FACE_OUTER_BOUND('',#2910,.T.);
#2009=FACE_OUTER_BOUND('',#2911,.T.);
#2010=FACE_OUTER_BOUND('',#2912,.T.);
#2011=FACE_OUTER_BOUND('',#2913,.T.);
#2012=FACE_OUTER_BOUND('',#2914,.T.);
#2013=FACE_OUTER_BOUND('',#2915,.T.);
#2014=FACE_OUTER_BOUND('',#2916,.T.);
#2015=FACE_OUTER_BOUND('',#2917,.T.);
#2016=FACE_OUTER_BOUND('',#2918,.T.);
#2017=FACE_OUTER_BOUND('',#2919,.T.);
#2018=FACE_OUTER_BOUND('',#2920,.T.);
#2019=FACE_OUTER_BOUND('',#2921,.T.);
#2904=EDGE_LOOP('',(#10956));
#2905=EDGE_LOOP('',(#10957,#10958,#10959,#10960));
#2906=EDGE_LOOP('',(#10961,#10962,#10963,#10964));
#2907=EDGE_LOOP('',(#10965,#10966,#10967,#10968));
#2908=EDGE_LOOP('',(#10969));
#2909=EDGE_LOOP('',(#10970));
#2910=EDGE_LOOP('',(#10971,#10972,#10973,#10974));
#2911=EDGE_LOOP('',(#10975,#10976,#10977,#10978));
#2912=EDGE_LOOP('',(#10979,#10980,#10981,#10982));
#2913=EDGE_LOOP('',(#10983));
#2914=EDGE_LOOP('',(#10984,#10985,#10986,#10987));
#2915=EDGE_LOOP('',(#10988,#10989,#10990,#10991));
#2916=EDGE_LOOP('',(#10992,#10993,#10994,#10995));
#2917=EDGE_LOOP('',(#10996,#10997,#10998,#10999));
#2918=EDGE_LOOP('',(#11000,#11001,#11002,#11003));
#2919=EDGE_LOOP('',(#11004,#11005,#11006,#11007));
#2920=EDGE_LOOP('',(#11008,#11009,#11010,#11011,#11012,#11013));
#2921=EDGE_LOOP('',(#11014,#11015,#11016,#11017,#11018,#11019));
#3659=LINE('',#23094,#4410);
#3660=LINE('',#23098,#4411);
#3661=LINE('',#23102,#4412);
#3662=LINE('',#23109,#4413);
#3663=LINE('',#23113,#4414);
#3664=LINE('',#23117,#4415);
#3665=LINE('',#23122,#4416);
#3666=LINE('',#23124,#4417);
#3667=LINE('',#23126,#4418);
#3668=LINE('',#23127,#4419);
#3669=LINE('',#23130,#4420);
#3670=LINE('',#23132,#4421);
#3671=LINE('',#23133,#4422);
#3672=LINE('',#23136,#4423);
#3673=LINE('',#23138,#4424);
#3674=LINE('',#23139,#4425);
#3675=LINE('',#23142,#4426);
#3676=LINE('',#23144,#4427);
#3677=LINE('',#23145,#4428);
#3678=LINE('',#23148,#4429);
#3679=LINE('',#23150,#4430);
#3680=LINE('',#23151,#4431);
#3681=LINE('',#23153,#4432);
#3682=LINE('',#23154,#4433);
#4410=VECTOR('',#18132,0.325);
#4411=VECTOR('',#18137,0.35);
#4412=VECTOR('',#18142,0.335);
#4413=VECTOR('',#18151,0.21);
#4414=VECTOR('',#18156,0.2);
#4415=VECTOR('',#18161,0.18);
#4416=VECTOR('',#18166,1.);
#4417=VECTOR('',#18167,1.);
#4418=VECTOR('',#18168,1.);
#4419=VECTOR('',#18169,1.);
#4420=VECTOR('',#18172,1.);
#4421=VECTOR('',#18173,1.);
#4422=VECTOR('',#18174,1.);
#4423=VECTOR('',#18177,1.);
#4424=VECTOR('',#18178,1.);
#4425=VECTOR('',#18179,1.);
#4426=VECTOR('',#18182,1.);
#4427=VECTOR('',#18183,1.);
#4428=VECTOR('',#18184,1.);
#4429=VECTOR('',#18187,1.);
#4430=VECTOR('',#18188,1.);
#4431=VECTOR('',#18189,1.);
#4432=VECTOR('',#18192,1.);
#4433=VECTOR('',#18193,1.);
#5204=CIRCLE('',#14335,0.3);
#5205=CIRCLE('',#14337,0.35);
#5206=CIRCLE('',#14339,0.35);
#5207=CIRCLE('',#14341,0.32);
#5208=CIRCLE('',#14343,0.22);
#5209=CIRCLE('',#14345,0.1954);
#5210=CIRCLE('',#14347,0.1954);
#5211=CIRCLE('',#14349,0.16);
#6263=VERTEX_POINT('',#23089);
#6264=VERTEX_POINT('',#23092);
#6265=VERTEX_POINT('',#23096);
#6266=VERTEX_POINT('',#23100);
#6267=VERTEX_POINT('',#23104);
#6268=VERTEX_POINT('',#23107);
#6269=VERTEX_POINT('',#23111);
#6270=VERTEX_POINT('',#23115);
#6271=VERTEX_POINT('',#23120);
#6272=VERTEX_POINT('',#23121);
#6273=VERTEX_POINT('',#23123);
#6274=VERTEX_POINT('',#23125);
#6275=VERTEX_POINT('',#23129);
#6276=VERTEX_POINT('',#23131);
#6277=VERTEX_POINT('',#23135);
#6278=VERTEX_POINT('',#23137);
#6279=VERTEX_POINT('',#23141);
#6280=VERTEX_POINT('',#23143);
#6281=VERTEX_POINT('',#23147);
#6282=VERTEX_POINT('',#23149);
#7837=EDGE_CURVE('',#6263,#6263,#5204,.T.);
#7838=EDGE_CURVE('',#6264,#6264,#5205,.T.);
#7839=EDGE_CURVE('',#6264,#6263,#3659,.T.);
#7840=EDGE_CURVE('',#6265,#6265,#5206,.T.);
#7841=EDGE_CURVE('',#6265,#6264,#3660,.T.);
#7842=EDGE_CURVE('',#6266,#6266,#5207,.T.);
#7843=EDGE_CURVE('',#6266,#6265,#3661,.T.);
#7844=EDGE_CURVE('',#6267,#6267,#5208,.T.);
#7845=EDGE_CURVE('',#6268,#6268,#5209,.F.);
#7846=EDGE_CURVE('',#6268,#6267,#3662,.T.);
#7847=EDGE_CURVE('',#6269,#6269,#5210,.F.);
#7848=EDGE_CURVE('',#6269,#6268,#3663,.T.);
#7849=EDGE_CURVE('',#6270,#6270,#5211,.T.);
#7850=EDGE_CURVE('',#6270,#6269,#3664,.T.);
#7851=EDGE_CURVE('',#6271,#6272,#3665,.T.);
#7852=EDGE_CURVE('',#6272,#6273,#3666,.T.);
#7853=EDGE_CURVE('',#6273,#6274,#3667,.T.);
#7854=EDGE_CURVE('',#6271,#6274,#3668,.T.);
#7855=EDGE_CURVE('',#6272,#6275,#3669,.T.);
#7856=EDGE_CURVE('',#6275,#6276,#3670,.T.);
#7857=EDGE_CURVE('',#6276,#6273,#3671,.T.);
#7858=EDGE_CURVE('',#6275,#6277,#3672,.T.);
#7859=EDGE_CURVE('',#6277,#6278,#3673,.T.);
#7860=EDGE_CURVE('',#6278,#6276,#3674,.T.);
#7861=EDGE_CURVE('',#6277,#6279,#3675,.T.);
#7862=EDGE_CURVE('',#6279,#6280,#3676,.T.);
#7863=EDGE_CURVE('',#6280,#6278,#3677,.T.);
#7864=EDGE_CURVE('',#6279,#6281,#3678,.T.);
#7865=EDGE_CURVE('',#6281,#6282,#3679,.T.);
#7866=EDGE_CURVE('',#6282,#6280,#3680,.T.);
#7867=EDGE_CURVE('',#6281,#6271,#3681,.T.);
#7868=EDGE_CURVE('',#6274,#6282,#3682,.T.);
#10956=ORIENTED_EDGE('',*,*,#7837,.F.);
#10957=ORIENTED_EDGE('',*,*,#7838,.F.);
#10958=ORIENTED_EDGE('',*,*,#7839,.T.);
#10959=ORIENTED_EDGE('',*,*,#7837,.T.);
#10960=ORIENTED_EDGE('',*,*,#7839,.F.);
#10961=ORIENTED_EDGE('',*,*,#7840,.F.);
#10962=ORIENTED_EDGE('',*,*,#7841,.T.);
#10963=ORIENTED_EDGE('',*,*,#7838,.T.);
#10964=ORIENTED_EDGE('',*,*,#7841,.F.);
#10965=ORIENTED_EDGE('',*,*,#7842,.F.);
#10966=ORIENTED_EDGE('',*,*,#7843,.T.);
#10967=ORIENTED_EDGE('',*,*,#7840,.T.);
#10968=ORIENTED_EDGE('',*,*,#7843,.F.);
#10969=ORIENTED_EDGE('',*,*,#7842,.T.);
#10970=ORIENTED_EDGE('',*,*,#7844,.F.);
#10971=ORIENTED_EDGE('',*,*,#7845,.F.);
#10972=ORIENTED_EDGE('',*,*,#7846,.T.);
#10973=ORIENTED_EDGE('',*,*,#7844,.T.);
#10974=ORIENTED_EDGE('',*,*,#7846,.F.);
#10975=ORIENTED_EDGE('',*,*,#7847,.F.);
#10976=ORIENTED_EDGE('',*,*,#7848,.T.);
#10977=ORIENTED_EDGE('',*,*,#7845,.T.);
#10978=ORIENTED_EDGE('',*,*,#7848,.F.);
#10979=ORIENTED_EDGE('',*,*,#7849,.F.);
#10980=ORIENTED_EDGE('',*,*,#7850,.T.);
#10981=ORIENTED_EDGE('',*,*,#7847,.T.);
#10982=ORIENTED_EDGE('',*,*,#7850,.F.);
#10983=ORIENTED_EDGE('',*,*,#7849,.T.);
#10984=ORIENTED_EDGE('',*,*,#7851,.T.);
#10985=ORIENTED_EDGE('',*,*,#7852,.T.);
#10986=ORIENTED_EDGE('',*,*,#7853,.T.);
#10987=ORIENTED_EDGE('',*,*,#7854,.F.);
#10988=ORIENTED_EDGE('',*,*,#7855,.T.);
#10989=ORIENTED_EDGE('',*,*,#7856,.T.);
#10990=ORIENTED_EDGE('',*,*,#7857,.T.);
#10991=ORIENTED_EDGE('',*,*,#7852,.F.);
#10992=ORIENTED_EDGE('',*,*,#7858,.T.);
#10993=ORIENTED_EDGE('',*,*,#7859,.T.);
#10994=ORIENTED_EDGE('',*,*,#7860,.T.);
#10995=ORIENTED_EDGE('',*,*,#7856,.F.);
#10996=ORIENTED_EDGE('',*,*,#7861,.T.);
#10997=ORIENTED_EDGE('',*,*,#7862,.T.);
#10998=ORIENTED_EDGE('',*,*,#7863,.T.);
#10999=ORIENTED_EDGE('',*,*,#7859,.F.);
#11000=ORIENTED_EDGE('',*,*,#7864,.T.);
#11001=ORIENTED_EDGE('',*,*,#7865,.T.);
#11002=ORIENTED_EDGE('',*,*,#7866,.T.);
#11003=ORIENTED_EDGE('',*,*,#7862,.F.);
#11004=ORIENTED_EDGE('',*,*,#7867,.T.);
#11005=ORIENTED_EDGE('',*,*,#7854,.T.);
#11006=ORIENTED_EDGE('',*,*,#7868,.T.);
#11007=ORIENTED_EDGE('',*,*,#7865,.F.);
#11008=ORIENTED_EDGE('',*,*,#7867,.F.);
#11009=ORIENTED_EDGE('',*,*,#7864,.F.);
#11010=ORIENTED_EDGE('',*,*,#7861,.F.);
#11011=ORIENTED_EDGE('',*,*,#7858,.F.);
#11012=ORIENTED_EDGE('',*,*,#7855,.F.);
#11013=ORIENTED_EDGE('',*,*,#7851,.F.);
#11014=ORIENTED_EDGE('',*,*,#7868,.F.);
#11015=ORIENTED_EDGE('',*,*,#7853,.F.);
#11016=ORIENTED_EDGE('',*,*,#7857,.F.);
#11017=ORIENTED_EDGE('',*,*,#7860,.F.);
#11018=ORIENTED_EDGE('',*,*,#7863,.F.);
#11019=ORIENTED_EDGE('',*,*,#7866,.F.);
#11479=CYLINDRICAL_SURFACE('',#14338,0.35);
#11480=CYLINDRICAL_SURFACE('',#14346,0.1954);
#12144=ADVANCED_FACE('',(#2003),#1319,.T.);
#12145=ADVANCED_FACE('',(#2004),#481,.T.);
#12146=ADVANCED_FACE('',(#2005),#11479,.T.);
#12147=ADVANCED_FACE('',(#2006),#482,.T.);
#12148=ADVANCED_FACE('',(#2007,#1026),#1320,.T.);
#12149=ADVANCED_FACE('',(#2008),#483,.T.);
#12150=ADVANCED_FACE('',(#2009),#11480,.T.);
#12151=ADVANCED_FACE('',(#2010),#484,.T.);
#12152=ADVANCED_FACE('',(#2011),#1321,.T.);
#12153=ADVANCED_FACE('',(#2012),#1322,.F.);
#12154=ADVANCED_FACE('',(#2013),#1323,.F.);
#12155=ADVANCED_FACE('',(#2014),#1324,.F.);
#12156=ADVANCED_FACE('',(#2015),#1325,.F.);
#12157=ADVANCED_FACE('',(#2016),#1326,.F.);
#12158=ADVANCED_FACE('',(#2017),#1327,.F.);
#12159=ADVANCED_FACE('',(#2018),#1328,.F.);
#12160=ADVANCED_FACE('',(#2019),#1329,.F.);
#12265=CLOSED_SHELL('',(#12144,#12145,#12146,#12147,#12148,#12149,#12150,
#12151,#12152));
#12266=CLOSED_SHELL('',(#12153,#12154,#12155,#12156,#12157,#12158,#12159,
#12160));
#14333=AXIS2_PLACEMENT_3D('',#23087,#18122,#18123);
#14334=AXIS2_PLACEMENT_3D('',#23088,#18124,#18125);
#14335=AXIS2_PLACEMENT_3D('',#23090,#18126,#18127);
#14336=AXIS2_PLACEMENT_3D('',#23091,#18128,#18129);
#14337=AXIS2_PLACEMENT_3D('',#23093,#18130,#18131);
#14338=AXIS2_PLACEMENT_3D('',#23095,#18133,#18134);
#14339=AXIS2_PLACEMENT_3D('',#23097,#18135,#18136);
#14340=AXIS2_PLACEMENT_3D('',#23099,#18138,#18139);
#14341=AXIS2_PLACEMENT_3D('',#23101,#18140,#18141);
#14342=AXIS2_PLACEMENT_3D('',#23103,#18143,#18144);
#14343=AXIS2_PLACEMENT_3D('',#23105,#18145,#18146);
#14344=AXIS2_PLACEMENT_3D('',#23106,#18147,#18148);
#14345=AXIS2_PLACEMENT_3D('',#23108,#18149,#18150);
#14346=AXIS2_PLACEMENT_3D('',#23110,#18152,#18153);
#14347=AXIS2_PLACEMENT_3D('',#23112,#18154,#18155);
#14348=AXIS2_PLACEMENT_3D('',#23114,#18157,#18158);
#14349=AXIS2_PLACEMENT_3D('',#23116,#18159,#18160);
#14350=AXIS2_PLACEMENT_3D('',#23118,#18162,#18163);
#14351=AXIS2_PLACEMENT_3D('',#23119,#18164,#18165);
#14352=AXIS2_PLACEMENT_3D('',#23128,#18170,#18171);
#14353=AXIS2_PLACEMENT_3D('',#23134,#18175,#18176);
#14354=AXIS2_PLACEMENT_3D('',#23140,#18180,#18181);
#14355=AXIS2_PLACEMENT_3D('',#23146,#18185,#18186);
#14356=AXIS2_PLACEMENT_3D('',#23152,#18190,#18191);
#14357=AXIS2_PLACEMENT_3D('',#23155,#18194,#18195);
#14358=AXIS2_PLACEMENT_3D('',#23156,#18196,#18197);
#18122=DIRECTION('axis',(0.,0.,1.));
#18123=DIRECTION('refdir',(1.,0.,0.));
#18124=DIRECTION('center_axis',(0.,1.,0.));
#18125=DIRECTION('ref_axis',(0.,0.,1.));
#18126=DIRECTION('center_axis',(0.,-1.,0.));
#18127=DIRECTION('ref_axis',(1.,0.,0.));
#18128=DIRECTION('center_axis',(0.,-1.,0.));
#18129=DIRECTION('ref_axis',(1.,0.,0.));
#18130=DIRECTION('center_axis',(0.,-1.,0.));
#18131=DIRECTION('ref_axis',(1.,0.,0.));
#18132=DIRECTION('',(0.707106781186547,0.707106781186548,8.65956056235493E-17));
#18133=DIRECTION('center_axis',(0.,-1.,0.));
#18134=DIRECTION('ref_axis',(1.,0.,0.));
#18135=DIRECTION('center_axis',(0.,-1.,0.));
#18136=DIRECTION('ref_axis',(1.,0.,0.));
#18137=DIRECTION('',(0.,1.,0.));
#18138=DIRECTION('center_axis',(0.,1.,0.));
#18139=DIRECTION('ref_axis',(1.,0.,0.));
#18140=DIRECTION('center_axis',(0.,-1.,0.));
#18141=DIRECTION('ref_axis',(1.,0.,0.));
#18142=DIRECTION('',(-0.707106781186547,0.707106781186548,-8.65956056235493E-17));
#18143=DIRECTION('center_axis',(0.,-1.,0.));
#18144=DIRECTION('ref_axis',(0.,0.,-1.));
#18145=DIRECTION('center_axis',(0.,-1.,0.));
#18146=DIRECTION('ref_axis',(1.,0.,0.));
#18147=DIRECTION('center_axis',(0.,1.,0.));
#18148=DIRECTION('ref_axis',(1.,0.,0.));
#18149=DIRECTION('center_axis',(0.,1.,0.));
#18150=DIRECTION('ref_axis',(1.,0.,0.));
#18151=DIRECTION('',(-0.447213595499958,0.894427190999916,-5.47678698264203E-17));
#18152=DIRECTION('center_axis',(0.,-1.,0.));
#18153=DIRECTION('ref_axis',(1.,0.,0.));
#18154=DIRECTION('center_axis',(0.,1.,0.));
#18155=DIRECTION('ref_axis',(1.,0.,0.));
#18156=DIRECTION('',(0.,1.,0.));
#18157=DIRECTION('center_axis',(0.,1.,0.));
#18158=DIRECTION('ref_axis',(1.,0.,0.));
#18159=DIRECTION('center_axis',(0.,-1.,0.));
#18160=DIRECTION('ref_axis',(1.,0.,0.));
#18161=DIRECTION('',(-0.707106781186547,0.707106781186548,-8.65956056235493E-17));
#18162=DIRECTION('center_axis',(0.,-1.,0.));
#18163=DIRECTION('ref_axis',(0.,0.,-1.));
#18164=DIRECTION('center_axis',(0.866025403784439,0.,-0.5));
#18165=DIRECTION('ref_axis',(0.5,0.,0.866025403784439));
#18166=DIRECTION('',(-0.5,0.,-0.866025403784439));
#18167=DIRECTION('',(0.,-1.,0.));
#18168=DIRECTION('',(0.5,0.,0.866025403784439));
#18169=DIRECTION('',(0.,-1.,0.));
#18170=DIRECTION('center_axis',(1.60246890531964E-16,0.,-1.));
#18171=DIRECTION('ref_axis',(1.,0.,1.60246890531964E-16));
#18172=DIRECTION('',(-1.,0.,-1.60246890531964E-16));
#18173=DIRECTION('',(0.,-1.,0.));
#18174=DIRECTION('',(1.,0.,1.60246890531964E-16));
#18175=DIRECTION('center_axis',(-0.866025403784439,0.,-0.5));
#18176=DIRECTION('ref_axis',(0.5,0.,-0.866025403784439));
#18177=DIRECTION('',(-0.5,0.,0.866025403784439));
#18178=DIRECTION('',(0.,-1.,0.));
#18179=DIRECTION('',(0.5,0.,-0.866025403784439));
#18180=DIRECTION('center_axis',(-0.866025403784439,0.,0.5));
#18181=DIRECTION('ref_axis',(-0.5,0.,-0.866025403784439));
#18182=DIRECTION('',(0.5,0.,0.866025403784439));
#18183=DIRECTION('',(0.,-1.,0.));
#18184=DIRECTION('',(-0.5,0.,-0.866025403784439));
#18185=DIRECTION('center_axis',(-1.60246890531964E-16,0.,1.));
#18186=DIRECTION('ref_axis',(-1.,0.,-1.60246890531964E-16));
#18187=DIRECTION('',(1.,0.,1.60246890531964E-16));
#18188=DIRECTION('',(0.,-1.,0.));
#18189=DIRECTION('',(-1.,0.,-1.60246890531964E-16));
#18190=DIRECTION('center_axis',(0.866025403784439,0.,0.5));
#18191=DIRECTION('ref_axis',(-0.5,0.,0.866025403784439));
#18192=DIRECTION('',(0.5,0.,-0.866025403784439));
#18193=DIRECTION('',(-0.5,0.,0.866025403784439));
#18194=DIRECTION('center_axis',(0.,1.,0.));
#18195=DIRECTION('ref_axis',(1.,0.,0.));
#18196=DIRECTION('center_axis',(0.,-1.,0.));
#18197=DIRECTION('ref_axis',(0.,0.,-1.));
#23087=CARTESIAN_POINT('',(0.,0.,0.));
#23088=CARTESIAN_POINT('Origin',(0.3,0.4,0.));
#23089=CARTESIAN_POINT('',(-0.3,0.4,-3.67394039744206E-17));
#23090=CARTESIAN_POINT('Origin',(0.,0.4,0.));
#23091=CARTESIAN_POINT('Origin',(0.,0.375,0.));
#23092=CARTESIAN_POINT('',(-0.35,0.35,-4.28626379701573E-17));
#23093=CARTESIAN_POINT('Origin',(0.,0.35,0.));
#23094=CARTESIAN_POINT('',(-0.325,0.375,-3.9801020972289E-17));
#23095=CARTESIAN_POINT('Origin',(0.,0.19,0.));
#23096=CARTESIAN_POINT('',(-0.35,0.03,-4.28626379701574E-17));
#23097=CARTESIAN_POINT('Origin',(0.,0.03,0.));
#23098=CARTESIAN_POINT('',(-0.35,0.19,-4.28626379701574E-17));
#23099=CARTESIAN_POINT('Origin',(0.,0.0149999999999999,0.));
#23100=CARTESIAN_POINT('',(-0.32,-3.29597460435593E-17,-3.91886975727153E-17));
#23101=CARTESIAN_POINT('Origin',(0.,0.,0.));
#23102=CARTESIAN_POINT('',(-0.335,0.0149999999999999,-4.10256677714363E-17));
#23103=CARTESIAN_POINT('Origin',(0.22,0.,0.));
#23104=CARTESIAN_POINT('',(-0.22,-6.93889390390723E-18,-2.69422295812418E-17));
#23105=CARTESIAN_POINT('Origin',(0.,0.,0.));
#23106=CARTESIAN_POINT('Origin',(0.,-0.02,0.));
#23107=CARTESIAN_POINT('',(-0.1954,-0.0492,2.39295984553393E-17));
#23108=CARTESIAN_POINT('Origin',(0.,-0.0492,0.));
#23109=CARTESIAN_POINT('',(-0.21,-0.02,-2.57175827820944E-17));
#23110=CARTESIAN_POINT('Origin',(0.,-0.8,0.));
#23111=CARTESIAN_POINT('',(-0.1954,-1.5646,2.39295984553393E-17));
#23112=CARTESIAN_POINT('Origin',(0.,-1.5646,0.));
#23113=CARTESIAN_POINT('',(-0.1954,-0.8,-2.39295984553393E-17));
#23114=CARTESIAN_POINT('Origin',(0.,-1.58,0.));
#23115=CARTESIAN_POINT('',(-0.16,-1.6,-1.95943487863577E-17));
#23116=CARTESIAN_POINT('Origin',(0.,-1.6,0.));
#23117=CARTESIAN_POINT('',(-0.18,-1.58,-2.20436423846524E-17));
#23118=CARTESIAN_POINT('Origin',(0.,-1.6,0.));
#23119=CARTESIAN_POINT('Origin',(0.0866025403784439,-0.4,-0.15));
#23120=CARTESIAN_POINT('',(0.173205080756888,-0.4,0.));
#23121=CARTESIAN_POINT('',(0.0866025403784439,-0.4,-0.15));
#23122=CARTESIAN_POINT('',(0.173205080756888,-0.4,0.));
#23123=CARTESIAN_POINT('',(0.0866025403784439,-0.64,-0.15));
#23124=CARTESIAN_POINT('',(0.0866025403784439,-0.4,-0.15));
#23125=CARTESIAN_POINT('',(0.173205080756888,-0.64,0.));
#23126=CARTESIAN_POINT('',(0.173205080756888,-0.64,0.));
#23127=CARTESIAN_POINT('',(0.173205080756888,-0.4,0.));
#23128=CARTESIAN_POINT('Origin',(-0.0866025403784438,-0.4,-0.15));
#23129=CARTESIAN_POINT('',(-0.0866025403784438,-0.4,-0.15));
#23130=CARTESIAN_POINT('',(0.0866025403784439,-0.4,-0.15));
#23131=CARTESIAN_POINT('',(-0.0866025403784438,-0.64,-0.15));
#23132=CARTESIAN_POINT('',(-0.0866025403784438,-0.4,-0.15));
#23133=CARTESIAN_POINT('',(0.0866025403784439,-0.64,-0.15));
#23134=CARTESIAN_POINT('Origin',(-0.173205080756888,-0.4,-2.77555756156289E-17));
#23135=CARTESIAN_POINT('',(-0.173205080756888,-0.4,-2.12115047744981E-17));
#23136=CARTESIAN_POINT('',(-0.0866025403784438,-0.4,-0.15));
#23137=CARTESIAN_POINT('',(-0.173205080756888,-0.64,-2.77555756156289E-17));
#23138=CARTESIAN_POINT('',(-0.173205080756888,-0.4,-2.12115047744981E-17));
#23139=CARTESIAN_POINT('',(-0.0866025403784438,-0.64,-0.15));
#23140=CARTESIAN_POINT('Origin',(-0.0866025403784439,-0.4,0.15));
#23141=CARTESIAN_POINT('',(-0.0866025403784439,-0.4,0.15));
#23142=CARTESIAN_POINT('',(-0.173205080756888,-0.4,-2.12115047744981E-17));
#23143=CARTESIAN_POINT('',(-0.0866025403784439,-0.64,0.15));
#23144=CARTESIAN_POINT('',(-0.0866025403784439,-0.4,0.15));
#23145=CARTESIAN_POINT('',(-0.173205080756888,-0.64,-2.12115047744981E-17));
#23146=CARTESIAN_POINT('Origin',(0.0866025403784439,-0.4,0.15));
#23147=CARTESIAN_POINT('',(0.0866025403784439,-0.4,0.15));
#23148=CARTESIAN_POINT('',(-0.0866025403784439,-0.4,0.15));
#23149=CARTESIAN_POINT('',(0.0866025403784439,-0.64,0.15));
#23150=CARTESIAN_POINT('',(0.0866025403784439,-0.4,0.15));
#23151=CARTESIAN_POINT('',(-0.0866025403784439,-0.64,0.15));
#23152=CARTESIAN_POINT('Origin',(0.173205080756888,-0.4,0.));
#23153=CARTESIAN_POINT('',(0.0866025403784439,-0.4,0.15));
#23154=CARTESIAN_POINT('',(0.0866025403784439,-0.64,0.15));
#23155=CARTESIAN_POINT('Origin',(0.,-0.4,-2.77555756156289E-17));
#23156=CARTESIAN_POINT('Origin',(0.,-0.64,-2.77555756156289E-17));
#23517=UNCERTAINTY_MEASURE_WITH_UNIT(LENGTH_MEASURE(0.001),#23588,
'DISTANCE_ACCURACY_VALUE',
'Maximum model space distance between geometric entities at asserted c
onnectivities');
#23522=UNCERTAINTY_MEASURE_WITH_UNIT(LENGTH_MEASURE(0.001),#23588,
'DISTANCE_ACCURACY_VALUE',
'Maximum model space distance between geometric entities at asserted c
onnectivities');
#23582=(
GEOMETRIC_REPRESENTATION_CONTEXT(3)
GLOBAL_UNCERTAINTY_ASSIGNED_CONTEXT((#23517))
GLOBAL_UNIT_ASSIGNED_CONTEXT((#23588,#23590,#23591))
REPRESENTATION_CONTEXT('','3D')
);
#23587=(
GEOMETRIC_REPRESENTATION_CONTEXT(3)
GLOBAL_UNCERTAINTY_ASSIGNED_CONTEXT((#23522))
GLOBAL_UNIT_ASSIGNED_CONTEXT((#23588,#23590,#23591))
REPRESENTATION_CONTEXT('','3D')
);
#23588=(
LENGTH_UNIT()
NAMED_UNIT(*)
SI_UNIT(.CENTI.,.METRE.)
);
#23590=(
NAMED_UNIT(*)
PLANE_ANGLE_UNIT()
SI_UNIT($,.RADIAN.)
);
#23591=(
NAMED_UNIT(*)
SI_UNIT($,.STERADIAN.)
SOLID_ANGLE_UNIT()
);
#23651=SHAPE_DEFINITION_REPRESENTATION(#23728,#23884);
#23728=PRODUCT_DEFINITION_SHAPE('',$,#23949);
#23884=SHAPE_REPRESENTATION('',(#14333),#23582);
#23889=PRODUCT_DEFINITION_CONTEXT('part definition',#24083,'design');
#23949=PRODUCT_DEFINITION('Cap Screw - M4x16','Cap Screw - M4x16',#24013,
#23889);
#24013=PRODUCT_DEFINITION_FORMATION('',$,#24144);
#24083=APPLICATION_CONTEXT(
'Core Data for Automotive Mechanical Design Process');
#24084=PRODUCT_CONTEXT('part definition',#24083,'mechanical');
#24144=PRODUCT('Cap Screw - M4x16','Cap Screw - M4x16',
'Cap Screw - M4x16',(#24084));
#24212=COLOUR_RGB('Black',0.12,0.14,0.17);
#24213=FILL_AREA_STYLE_COLOUR('',#24212);
#24214=FILL_AREA_STYLE('',(#24213));
#24215=SURFACE_STYLE_FILL_AREA(#24214);
#24216=SURFACE_SIDE_STYLE('',(#24215));
#24217=SURFACE_STYLE_USAGE(.BOTH.,#24216);
#24218=PRESENTATION_STYLE_ASSIGNMENT((#24217));
ENDSEC;
END-ISO-10303-21;
